ISO-10303-21;
HEADER;
/* Generated by software containing ST-Developer
 * from STEP Tools, Inc. (www.steptools.com) 
 */

FILE_DESCRIPTION(
/* description */ ('Guided pneumatic stop gate'),
/* implementation_level */ '2;1');

FILE_NAME(
/* name */ 'M4x10 Cap Screw.step',
/* time_stamp */ '2026-10-27T21:43:45-07:00',
/* author */ (''),
/* organization */ (''),
/* preprocessor_version */ 'ST-DEVELOPER v20.2',
/* originating_system */ 'Autodesk Translation Framework v15.17.0.0',
/* authorisation */ '');

FILE_SCHEMA (('AUTOMOTIVE_DESIGN { 1 0 10303 214 3 1 1 }'));
ENDSEC;

DATA;
#10=MECHANICAL_DESIGN_GEOMETRIC_PRESENTATION_REPRESENTATION('',(#561),#14392);
#416=ORIENTED_CLOSED_SHELL('',*,#7902,.F.);
#420=BREP_WITH_VOIDS('Body1',#7903,(#416));
#434=CONICAL_SURFACE('',#9045,0.325,0.785398163397448);
#435=CONICAL_SURFACE('',#9049,0.335,0.785398163397448);
#436=CONICAL_SURFACE('',#9053,0.21,0.463647609000806);
#477=SHAPE_REPRESENTATION_RELATIONSHIP('SRR','None',#14613,#519);
#519=ADVANCED_BREP_SHAPE_REPRESENTATION('',(#420),#14375);
#561=STYLED_ITEM('',(#14898),#420);
#788=FACE_BOUND('',#2103,.T.);
#1020=PLANE('',#9033);
#1021=PLANE('',#9034);
#1022=PLANE('',#9035);
#1023=PLANE('',#9036);
#1024=PLANE('',#9037);
#1025=PLANE('',#9038);
#1026=PLANE('',#9039);
#1027=PLANE('',#9040);
#1028=PLANE('',#9041);
#1029=PLANE('',#9043);
#1030=PLANE('',#9051);
#1441=FACE_OUTER_BOUND('',#2089,.T.);
#1442=FACE_OUTER_BOUND('',#2090,.T.);
#1443=FACE_OUTER_BOUND('',#2091,.T.);
#1444=FACE_OUTER_BOUND('',#2092,.T.);
#1445=FACE_OUTER_BOUND('',#2093,.T.);
#1446=FACE_OUTER_BOUND('',#2094,.T.);
#1447=FACE_OUTER_BOUND('',#2095,.T.);
#1448=FACE_OUTER_BOUND('',#2096,.T.);
#1449=FACE_OUTER_BOUND('',#2097,.T.);
#1450=FACE_OUTER_BOUND('',#2098,.T.);
#1451=FACE_OUTER_BOUND('',#2099,.T.);
#1452=FACE_OUTER_BOUND('',#2100,.T.);
#1453=FACE_OUTER_BOUND('',#2101,.T.);
#1454=FACE_OUTER_BOUND('',#2102,.T.);
#1455=FACE_OUTER_BOUND('',#2104,.T.);
#1456=FACE_OUTER_BOUND('',#2105,.T.);
#2089=EDGE_LOOP('',(#6642,#6643,#6644,#6645));
#2090=EDGE_LOOP('',(#6646,#6647,#6648,#6649));
#2091=EDGE_LOOP('',(#6650,#6651,#6652,#6653));
#2092=EDGE_LOOP('',(#6654,#6655,#6656,#6657));
#2093=EDGE_LOOP('',(#6658,#6659,#6660,#6661));
#2094=EDGE_LOOP('',(#6662,#6663,#6664,#6665));
#2095=EDGE_LOOP('',(#6666,#6667,#6668,#6669,#6670,#6671));
#2096=EDGE_LOOP('',(#6672,#6673,#6674,#6675,#6676,#6677));
#2097=EDGE_LOOP('',(#6678));
#2098=EDGE_LOOP('',(#6679));
#2099=EDGE_LOOP('',(#6680,#6681,#6682,#6683));
#2100=EDGE_LOOP('',(#6684,#6685,#6686,#6687));
#2101=EDGE_LOOP('',(#6688,#6689,#6690,#6691));
#2102=EDGE_LOOP('',(#6692));
#2103=EDGE_LOOP('',(#6693));
#2104=EDGE_LOOP('',(#6694,#6695,#6696,#6697));
#2105=EDGE_LOOP('',(#6698,#6699,#6700,#6701));
#2638=LINE('',#13395,#3183);
#2639=LINE('',#13397,#3184);
#2640=LINE('',#13399,#3185);
#2641=LINE('',#13400,#3186);
#2642=LINE('',#13403,#3187);
#2643=LINE('',#13405,#3188);
#2644=LINE('',#13406,#3189);
#2645=LINE('',#13409,#3190);
#2646=LINE('',#13411,#3191);
#2647=LINE('',#13412,#3192);
#2648=LINE('',#13415,#3193);
#2649=LINE('',#13417,#3194);
#2650=LINE('',#13418,#3195);
#2651=LINE('',#13421,#3196);
#2652=LINE('',#13423,#3197);
#2653=LINE('',#13424,#3198);
#2654=LINE('',#13426,#3199);
#2655=LINE('',#13427,#3200);
#2656=LINE('',#13439,#3201);
#2657=LINE('',#13443,#3202);
#2658=LINE('',#13447,#3203);
#2659=LINE('',#13454,#3204);
#2660=LINE('',#13456,#3205);
#3183=VECTOR('',#11041,1.);
#3184=VECTOR('',#11042,1.);
#3185=VECTOR('',#11043,1.);
#3186=VECTOR('',#11044,1.);
#3187=VECTOR('',#11047,1.);
#3188=VECTOR('',#11048,1.);
#3189=VECTOR('',#11049,1.);
#3190=VECTOR('',#11052,1.);
#3191=VECTOR('',#11053,1.);
#3192=VECTOR('',#11054,1.);
#3193=VECTOR('',#11057,1.);
#3194=VECTOR('',#11058,1.);
#3195=VECTOR('',#11059,1.);
#3196=VECTOR('',#11062,1.);
#3197=VECTOR('',#11063,1.);
#3198=VECTOR('',#11064,1.);
#3199=VECTOR('',#11067,1.);
#3200=VECTOR('',#11068,1.);
#3201=VECTOR('',#11085,0.325);
#3202=VECTOR('',#11090,0.35);
#3203=VECTOR('',#11095,0.335);
#3204=VECTOR('',#11104,0.21);
#3205=VECTOR('',#11107,0.2);
#3645=CIRCLE('',#9042,0.1954);
#3646=CIRCLE('',#9044,0.3);
#3647=CIRCLE('',#9046,0.35);
#3648=CIRCLE('',#9048,0.35);
#3649=CIRCLE('',#9050,0.32);
#3650=CIRCLE('',#9052,0.22);
#3651=CIRCLE('',#9054,0.1954);
#4164=VERTEX_POINT('',#13393);
#4165=VERTEX_POINT('',#13394);
#4166=VERTEX_POINT('',#13396);
#4167=VERTEX_POINT('',#13398);
#4168=VERTEX_POINT('',#13402);
#4169=VERTEX_POINT('',#13404);
#4170=VERTEX_POINT('',#13408);
#4171=VERTEX_POINT('',#13410);
#4172=VERTEX_POINT('',#13414);
#4173=VERTEX_POINT('',#13416);
#4174=VERTEX_POINT('',#13420);
#4175=VERTEX_POINT('',#13422);
#4176=VERTEX_POINT('',#13431);
#4177=VERTEX_POINT('',#13434);
#4178=VERTEX_POINT('',#13437);
#4179=VERTEX_POINT('',#13441);
#4180=VERTEX_POINT('',#13445);
#4181=VERTEX_POINT('',#13449);
#4182=VERTEX_POINT('',#13452);
#5019=EDGE_CURVE('',#4164,#4165,#2638,.T.);
#5020=EDGE_CURVE('',#4165,#4166,#2639,.T.);
#5021=EDGE_CURVE('',#4166,#4167,#2640,.T.);
#5022=EDGE_CURVE('',#4164,#4167,#2641,.T.);
#5023=EDGE_CURVE('',#4165,#4168,#2642,.T.);
#5024=EDGE_CURVE('',#4168,#4169,#2643,.T.);
#5025=EDGE_CURVE('',#4169,#4166,#2644,.T.);
#5026=EDGE_CURVE('',#4168,#4170,#2645,.T.);
#5027=EDGE_CURVE('',#4170,#4171,#2646,.T.);
#5028=EDGE_CURVE('',#4171,#4169,#2647,.T.);
#5029=EDGE_CURVE('',#4170,#4172,#2648,.T.);
#5030=EDGE_CURVE('',#4172,#4173,#2649,.T.);
#5031=EDGE_CURVE('',#4173,#4171,#2650,.T.);
#5032=EDGE_CURVE('',#4172,#4174,#2651,.T.);
#5033=EDGE_CURVE('',#4174,#4175,#2652,.T.);
#5034=EDGE_CURVE('',#4175,#4173,#2653,.T.);
#5035=EDGE_CURVE('',#4174,#4164,#2654,.T.);
#5036=EDGE_CURVE('',#4167,#4175,#2655,.T.);
#5037=EDGE_CURVE('',#4176,#4176,#3645,.T.);
#5038=EDGE_CURVE('',#4177,#4177,#3646,.T.);
#5039=EDGE_CURVE('',#4178,#4178,#3647,.T.);
#5040=EDGE_CURVE('',#4178,#4177,#2656,.T.);
#5041=EDGE_CURVE('',#4179,#4179,#3648,.T.);
#5042=EDGE_CURVE('',#4179,#4178,#2657,.T.);
#5043=EDGE_CURVE('',#4180,#4180,#3649,.T.);
#5044=EDGE_CURVE('',#4180,#4179,#2658,.T.);
#5045=EDGE_CURVE('',#4181,#4181,#3650,.T.);
#5046=EDGE_CURVE('',#4182,#4182,#3651,.F.);
#5047=EDGE_CURVE('',#4182,#4181,#2659,.T.);
#5048=EDGE_CURVE('',#4176,#4182,#2660,.T.);
#6642=ORIENTED_EDGE('',*,*,#5019,.T.);
#6643=ORIENTED_EDGE('',*,*,#5020,.T.);
#6644=ORIENTED_EDGE('',*,*,#5021,.T.);
#6645=ORIENTED_EDGE('',*,*,#5022,.F.);
#6646=ORIENTED_EDGE('',*,*,#5023,.T.);
#6647=ORIENTED_EDGE('',*,*,#5024,.T.);
#6648=ORIENTED_EDGE('',*,*,#5025,.T.);
#6649=ORIENTED_EDGE('',*,*,#5020,.F.);
#6650=ORIENTED_EDGE('',*,*,#5026,.T.);
#6651=ORIENTED_EDGE('',*,*,#5027,.T.);
#6652=ORIENTED_EDGE('',*,*,#5028,.T.);
#6653=ORIENTED_EDGE('',*,*,#5024,.F.);
#6654=ORIENTED_EDGE('',*,*,#5029,.T.);
#6655=ORIENTED_EDGE('',*,*,#5030,.T.);
#6656=ORIENTED_EDGE('',*,*,#5031,.T.);
#6657=ORIENTED_EDGE('',*,*,#5027,.F.);
#6658=ORIENTED_EDGE('',*,*,#5032,.T.);
#6659=ORIENTED_EDGE('',*,*,#5033,.T.);
#6660=ORIENTED_EDGE('',*,*,#5034,.T.);
#6661=ORIENTED_EDGE('',*,*,#5030,.F.);
#6662=ORIENTED_EDGE('',*,*,#5035,.T.);
#6663=ORIENTED_EDGE('',*,*,#5022,.T.);
#6664=ORIENTED_EDGE('',*,*,#5036,.T.);
#6665=ORIENTED_EDGE('',*,*,#5033,.F.);
#6666=ORIENTED_EDGE('',*,*,#5035,.F.);
#6667=ORIENTED_EDGE('',*,*,#5032,.F.);
#6668=ORIENTED_EDGE('',*,*,#5029,.F.);
#6669=ORIENTED_EDGE('',*,*,#5026,.F.);
#6670=ORIENTED_EDGE('',*,*,#5023,.F.);
#6671=ORIENTED_EDGE('',*,*,#5019,.F.);
#6672=ORIENTED_EDGE('',*,*,#5036,.F.);
#6673=ORIENTED_EDGE('',*,*,#5021,.F.);
#6674=ORIENTED_EDGE('',*,*,#5025,.F.);
#6675=ORIENTED_EDGE('',*,*,#5028,.F.);
#6676=ORIENTED_EDGE('',*,*,#5031,.F.);
#6677=ORIENTED_EDGE('',*,*,#5034,.F.);
#6678=ORIENTED_EDGE('',*,*,#5037,.F.);
#6679=ORIENTED_EDGE('',*,*,#5038,.F.);
#6680=ORIENTED_EDGE('',*,*,#5039,.F.);
#6681=ORIENTED_EDGE('',*,*,#5040,.T.);
#6682=ORIENTED_EDGE('',*,*,#5038,.T.);
#6683=ORIENTED_EDGE('',*,*,#5040,.F.);
#6684=ORIENTED_EDGE('',*,*,#5041,.F.);
#6685=ORIENTED_EDGE('',*,*,#5042,.T.);
#6686=ORIENTED_EDGE('',*,*,#5039,.T.);
#6687=ORIENTED_EDGE('',*,*,#5042,.F.);
#6688=ORIENTED_EDGE('',*,*,#5043,.F.);
#6689=ORIENTED_EDGE('',*,*,#5044,.T.);
#6690=ORIENTED_EDGE('',*,*,#5041,.T.);
#6691=ORIENTED_EDGE('',*,*,#5044,.F.);
#6692=ORIENTED_EDGE('',*,*,#5043,.T.);
#6693=ORIENTED_EDGE('',*,*,#5045,.F.);
#6694=ORIENTED_EDGE('',*,*,#5046,.F.);
#6695=ORIENTED_EDGE('',*,*,#5047,.T.);
#6696=ORIENTED_EDGE('',*,*,#5045,.T.);
#6697=ORIENTED_EDGE('',*,*,#5047,.F.);
#6698=ORIENTED_EDGE('',*,*,#5037,.T.);
#6699=ORIENTED_EDGE('',*,*,#5048,.T.);
#6700=ORIENTED_EDGE('',*,*,#5046,.T.);
#6701=ORIENTED_EDGE('',*,*,#5048,.F.);
#7365=CYLINDRICAL_SURFACE('',#9047,0.35);
#7366=CYLINDRICAL_SURFACE('',#9055,0.1954);
#7723=ADVANCED_FACE('',(#1441),#1020,.F.);
#7724=ADVANCED_FACE('',(#1442),#1021,.F.);
#7725=ADVANCED_FACE('',(#1443),#1022,.F.);
#7726=ADVANCED_FACE('',(#1444),#1023,.F.);
#7727=ADVANCED_FACE('',(#1445),#1024,.F.);
#7728=ADVANCED_FACE('',(#1446),#1025,.F.);
#7729=ADVANCED_FACE('',(#1447),#1026,.F.);
#7730=ADVANCED_FACE('',(#1448),#1027,.F.);
#7731=ADVANCED_FACE('',(#1449),#1028,.F.);
#7732=ADVANCED_FACE('',(#1450),#1029,.T.);
#7733=ADVANCED_FACE('',(#1451),#434,.T.);
#7734=ADVANCED_FACE('',(#1452),#7365,.T.);
#7735=ADVANCED_FACE('',(#1453),#435,.T.);
#7736=ADVANCED_FACE('',(#1454,#788),#1030,.T.);
#7737=ADVANCED_FACE('',(#1455),#436,.T.);
#7738=ADVANCED_FACE('',(#1456),#7366,.T.);
#7902=CLOSED_SHELL('',(#7723,#7724,#7725,#7726,#7727,#7728,#7729,#7730));
#7903=CLOSED_SHELL('',(#7731,#7732,#7733,#7734,#7735,#7736,#7737,#7738));
#9032=AXIS2_PLACEMENT_3D('',#13391,#11037,#11038);
#9033=AXIS2_PLACEMENT_3D('',#13392,#11039,#11040);
#9034=AXIS2_PLACEMENT_3D('',#13401,#11045,#11046);
#9035=AXIS2_PLACEMENT_3D('',#13407,#11050,#11051);
#9036=AXIS2_PLACEMENT_3D('',#13413,#11055,#11056);
#9037=AXIS2_PLACEMENT_3D('',#13419,#11060,#11061);
#9038=AXIS2_PLACEMENT_3D('',#13425,#11065,#11066);
#9039=AXIS2_PLACEMENT_3D('',#13428,#11069,#11070);
#9040=AXIS2_PLACEMENT_3D('',#13429,#11071,#11072);
#9041=AXIS2_PLACEMENT_3D('',#13430,#11073,#11074);
#9042=AXIS2_PLACEMENT_3D('',#13432,#11075,#11076);
#9043=AXIS2_PLACEMENT_3D('',#13433,#11077,#11078);
#9044=AXIS2_PLACEMENT_3D('',#13435,#11079,#11080);
#9045=AXIS2_PLACEMENT_3D('',#13436,#11081,#11082);
#9046=AXIS2_PLACEMENT_3D('',#13438,#11083,#11084);
#9047=AXIS2_PLACEMENT_3D('',#13440,#11086,#11087);
#9048=AXIS2_PLACEMENT_3D('',#13442,#11088,#11089);
#9049=AXIS2_PLACEMENT_3D('',#13444,#11091,#11092);
#9050=AXIS2_PLACEMENT_3D('',#13446,#11093,#11094);
#9051=AXIS2_PLACEMENT_3D('',#13448,#11096,#11097);
#9052=AXIS2_PLACEMENT_3D('',#13450,#11098,#11099);
#9053=AXIS2_PLACEMENT_3D('',#13451,#11100,#11101);
#9054=AXIS2_PLACEMENT_3D('',#13453,#11102,#11103);
#9055=AXIS2_PLACEMENT_3D('',#13455,#11105,#11106);
#11037=DIRECTION('axis',(0.,0.,1.));
#11038=DIRECTION('refdir',(1.,0.,0.));
#11039=DIRECTION('center_axis',(0.866025403784439,0.,-0.5));
#11040=DIRECTION('ref_axis',(0.5,0.,0.866025403784439));
#11041=DIRECTION('',(-0.5,0.,-0.866025403784439));
#11042=DIRECTION('',(0.,-1.,0.));
#11043=DIRECTION('',(0.5,0.,0.866025403784439));
#11044=DIRECTION('',(0.,-1.,0.));
#11045=DIRECTION('center_axis',(1.60246890531964E-16,0.,-1.));
#11046=DIRECTION('ref_axis',(1.,0.,1.60246890531964E-16));
#11047=DIRECTION('',(-1.,0.,-1.60246890531964E-16));
#11048=DIRECTION('',(0.,-1.,0.));
#11049=DIRECTION('',(1.,0.,1.60246890531964E-16));
#11050=DIRECTION('center_axis',(-0.866025403784439,0.,-0.5));
#11051=DIRECTION('ref_axis',(0.5,0.,-0.866025403784439));
#11052=DIRECTION('',(-0.5,0.,0.866025403784439));
#11053=DIRECTION('',(0.,-1.,0.));
#11054=DIRECTION('',(0.5,0.,-0.866025403784439));
#11055=DIRECTION('center_axis',(-0.866025403784439,0.,0.5));
#11056=DIRECTION('ref_axis',(-0.5,0.,-0.866025403784439));
#11057=DIRECTION('',(0.5,0.,0.866025403784439));
#11058=DIRECTION('',(0.,-1.,0.));
#11059=DIRECTION('',(-0.5,0.,-0.866025403784439));
#11060=DIRECTION('center_axis',(-1.60246890531964E-16,0.,1.));
#11061=DIRECTION('ref_axis',(-1.,0.,-1.60246890531964E-16));
#11062=DIRECTION('',(1.,0.,1.60246890531964E-16));
#11063=DIRECTION('',(0.,-1.,0.));
#11064=DIRECTION('',(-1.,0.,-1.60246890531964E-16));
#11065=DIRECTION('center_axis',(0.866025403784439,0.,0.5));
#11066=DIRECTION('ref_axis',(-0.5,0.,0.866025403784439));
#11067=DIRECTION('',(0.5,0.,-0.866025403784439));
#11068=DIRECTION('',(-0.5,0.,0.866025403784439));
#11069=DIRECTION('center_axis',(0.,1.,0.));
#11070=DIRECTION('ref_axis',(1.,0.,0.));
#11071=DIRECTION('center_axis',(0.,-1.,0.));
#11072=DIRECTION('ref_axis',(0.,0.,-1.));
#11073=DIRECTION('center_axis',(0.,1.,0.));
#11074=DIRECTION('ref_axis',(1.,0.,0.));
#11075=DIRECTION('center_axis',(0.,1.,0.));
#11076=DIRECTION('ref_axis',(1.,0.,0.));
#11077=DIRECTION('center_axis',(0.,1.,0.));
#11078=DIRECTION('ref_axis',(0.,0.,1.));
#11079=DIRECTION('center_axis',(0.,-1.,0.));
#11080=DIRECTION('ref_axis',(1.,0.,0.));
#11081=DIRECTION('center_axis',(0.,-1.,0.));
#11082=DIRECTION('ref_axis',(1.,0.,0.));
#11083=DIRECTION('center_axis',(0.,-1.,0.));
#11084=DIRECTION('ref_axis',(1.,0.,0.));
#11085=DIRECTION('',(0.707106781186547,0.707106781186548,8.65956056235493E-17));
#11086=DIRECTION('center_axis',(0.,-1.,0.));
#11087=DIRECTION('ref_axis',(1.,0.,0.));
#11088=DIRECTION('center_axis',(0.,-1.,0.));
#11089=DIRECTION('ref_axis',(1.,0.,0.));
#11090=DIRECTION('',(0.,1.,0.));
#11091=DIRECTION('center_axis',(0.,1.,0.));
#11092=DIRECTION('ref_axis',(1.,0.,0.));
#11093=DIRECTION('center_axis',(0.,-1.,0.));
#11094=DIRECTION('ref_axis',(1.,0.,0.));
#11095=DIRECTION('',(-0.707106781186547,0.707106781186548,-8.65956056235493E-17));
#11096=DIRECTION('center_axis',(0.,-1.,0.));
#11097=DIRECTION('ref_axis',(0.,0.,-1.));
#11098=DIRECTION('center_axis',(0.,-1.,0.));
#11099=DIRECTION('ref_axis',(1.,0.,0.));
#11100=DIRECTION('center_axis',(0.,1.,0.));
#11101=DIRECTION('ref_axis',(1.,0.,0.));
#11102=DIRECTION('center_axis',(0.,1.,0.));
#11103=DIRECTION('ref_axis',(1.,0.,0.));
#11104=DIRECTION('',(-0.447213595499958,0.894427190999916,-5.47678698264203E-17));
#11105=DIRECTION('center_axis',(0.,-1.,0.));
#11106=DIRECTION('ref_axis',(1.,0.,0.));
#11107=DIRECTION('',(0.,1.,0.));
#13391=CARTESIAN_POINT('',(0.,0.,0.));
#13392=CARTESIAN_POINT('Origin',(0.0866025403784439,-0.4,-0.15));
#13393=CARTESIAN_POINT('',(0.173205080756888,-0.4,0.));
#13394=CARTESIAN_POINT('',(0.0866025403784439,-0.4,-0.15));
#13395=CARTESIAN_POINT('',(0.173205080756888,-0.4,0.));
#13396=CARTESIAN_POINT('',(0.0866025403784439,-0.64,-0.15));
#13397=CARTESIAN_POINT('',(0.0866025403784439,-0.4,-0.15));
#13398=CARTESIAN_POINT('',(0.173205080756888,-0.64,0.));
#13399=CARTESIAN_POINT('',(0.173205080756888,-0.64,0.));
#13400=CARTESIAN_POINT('',(0.173205080756888,-0.4,0.));
#13401=CARTESIAN_POINT('Origin',(-0.0866025403784438,-0.4,-0.15));
#13402=CARTESIAN_POINT('',(-0.0866025403784438,-0.4,-0.15));
#13403=CARTESIAN_POINT('',(0.0866025403784439,-0.4,-0.15));
#13404=CARTESIAN_POINT('',(-0.0866025403784438,-0.64,-0.15));
#13405=CARTESIAN_POINT('',(-0.0866025403784438,-0.4,-0.15));
#13406=CARTESIAN_POINT('',(0.0866025403784439,-0.64,-0.15));
#13407=CARTESIAN_POINT('Origin',(-0.173205080756888,-0.4,-2.77555756156289E-17));
#13408=CARTESIAN_POINT('',(-0.173205080756888,-0.4,-2.12115047744981E-17));
#13409=CARTESIAN_POINT('',(-0.0866025403784438,-0.4,-0.15));
#13410=CARTESIAN_POINT('',(-0.173205080756888,-0.64,-2.77555756156289E-17));
#13411=CARTESIAN_POINT('',(-0.173205080756888,-0.4,-2.12115047744981E-17));
#13412=CARTESIAN_POINT('',(-0.0866025403784438,-0.64,-0.15));
#13413=CARTESIAN_POINT('Origin',(-0.0866025403784439,-0.4,0.15));
#13414=CARTESIAN_POINT('',(-0.0866025403784439,-0.4,0.15));
#13415=CARTESIAN_POINT('',(-0.173205080756888,-0.4,-2.12115047744981E-17));
#13416=CARTESIAN_POINT('',(-0.0866025403784439,-0.64,0.15));
#13417=CARTESIAN_POINT('',(-0.0866025403784439,-0.4,0.15));
#13418=CARTESIAN_POINT('',(-0.173205080756888,-0.64,-2.12115047744981E-17));
#13419=CARTESIAN_POINT('Origin',(0.0866025403784439,-0.4,0.15));
#13420=CARTESIAN_POINT('',(0.0866025403784439,-0.4,0.15));
#13421=CARTESIAN_POINT('',(-0.0866025403784439,-0.4,0.15));
#13422=CARTESIAN_POINT('',(0.0866025403784439,-0.64,0.15));
#13423=CARTESIAN_POINT('',(0.0866025403784439,-0.4,0.15));
#13424=CARTESIAN_POINT('',(-0.0866025403784439,-0.64,0.15));
#13425=CARTESIAN_POINT('Origin',(0.173205080756888,-0.4,0.));
#13426=CARTESIAN_POINT('',(0.0866025403784439,-0.4,0.15));
#13427=CARTESIAN_POINT('',(0.0866025403784439,-0.64,0.15));
#13428=CARTESIAN_POINT('Origin',(0.,-0.4,-2.77555756156289E-17));
#13429=CARTESIAN_POINT('Origin',(0.,-0.64,-2.77555756156289E-17));
#13430=CARTESIAN_POINT('Origin',(0.,-1.,0.));
#13431=CARTESIAN_POINT('',(-0.1954,-1.,2.39295984553393E-17));
#13432=CARTESIAN_POINT('Origin',(0.,-1.,0.));
#13433=CARTESIAN_POINT('Origin',(0.3,0.4,0.));
#13434=CARTESIAN_POINT('',(-0.3,0.4,-3.67394039744206E-17));
#13435=CARTESIAN_POINT('Origin',(0.,0.4,0.));
#13436=CARTESIAN_POINT('Origin',(0.,0.375,0.));
#13437=CARTESIAN_POINT('',(-0.35,0.35,-4.28626379701573E-17));
#13438=CARTESIAN_POINT('Origin',(0.,0.35,0.));
#13439=CARTESIAN_POINT('',(-0.325,0.375,-3.9801020972289E-17));
#13440=CARTESIAN_POINT('Origin',(0.,0.19,0.));
#13441=CARTESIAN_POINT('',(-0.35,0.03,-4.28626379701574E-17));
#13442=CARTESIAN_POINT('Origin',(0.,0.03,0.));
#13443=CARTESIAN_POINT('',(-0.35,0.19,-4.28626379701574E-17));
#13444=CARTESIAN_POINT('Origin',(0.,0.0149999999999999,0.));
#13445=CARTESIAN_POINT('',(-0.32,-3.29597460435593E-17,-3.91886975727153E-17));
#13446=CARTESIAN_POINT('Origin',(0.,0.,0.));
#13447=CARTESIAN_POINT('',(-0.335,0.0149999999999999,-4.10256677714363E-17));
#13448=CARTESIAN_POINT('Origin',(0.22,0.,0.));
#13449=CARTESIAN_POINT('',(-0.22,-6.93889390390723E-18,-2.69422295812418E-17));
#13450=CARTESIAN_POINT('Origin',(0.,0.,0.));
#13451=CARTESIAN_POINT('Origin',(0.,-0.02,0.));
#13452=CARTESIAN_POINT('',(-0.1954,-0.0492,2.39295984553393E-17));
#13453=CARTESIAN_POINT('Origin',(0.,-0.0492,0.));
#13454=CARTESIAN_POINT('',(-0.21,-0.02,-2.57175827820944E-17));
#13455=CARTESIAN_POINT('Origin',(0.,-0.8,0.));
#13456=CARTESIAN_POINT('',(-0.1954,-0.8,-2.39295984553393E-17));
#14327=UNCERTAINTY_MEASURE_WITH_UNIT(LENGTH_MEASURE(0.001),#14393,
'DISTANCE_ACCURACY_VALUE',
'Maximum model space distance between geometric entities at asserted c
onnectivities');
#14344=UNCERTAINTY_MEASURE_WITH_UNIT(LENGTH_MEASURE(0.001),#14393,
'DISTANCE_ACCURACY_VALUE',
'Maximum model space distance between geometric entities at asserted c
onnectivities');
#14375=(
GEOMETRIC_REPRESENTATION_CONTEXT(3)
GLOBAL_UNCERTAINTY_ASSIGNED_CONTEXT((#14327))
GLOBAL_UNIT_ASSIGNED_CONTEXT((#14393,#14395,#14396))
REPRESENTATION_CONTEXT('','3D')
);
#14392=(
GEOMETRIC_REPRESENTATION_CONTEXT(3)
GLOBAL_UNCERTAINTY_ASSIGNED_CONTEXT((#14344))
GLOBAL_UNIT_ASSIGNED_CONTEXT((#14393,#14395,#14396))
REPRESENTATION_CONTEXT('','3D')
);
#14393=(
LENGTH_UNIT()
NAMED_UNIT(*)
SI_UNIT(.CENTI.,.METRE.)
);
#14395=(
NAMED_UNIT(*)
PLANE_ANGLE_UNIT()
SI_UNIT($,.RADIAN.)
);
#14396=(
NAMED_UNIT(*)
SI_UNIT($,.STERADIAN.)
SOLID_ANGLE_UNIT()
);
#14427=SHAPE_DEFINITION_REPRESENTATION(#14478,#14613);
#14478=PRODUCT_DEFINITION_SHAPE('',$,#14661);
#14613=SHAPE_REPRESENTATION('',(#9032),#14375);
#14630=PRODUCT_DEFINITION_CONTEXT('part definition',#14773,'design');
#14661=PRODUCT_DEFINITION('M4x10 Cap Screw','M4x10 Cap Screw',#14708,#14630);
#14708=PRODUCT_DEFINITION_FORMATION('',$,#14805);
#14773=APPLICATION_CONTEXT(
'Core Data for Automotive Mechanical Design Process');
#14774=PRODUCT_CONTEXT('part definition',#14773,'mechanical');
#14805=PRODUCT('M4x10 Cap Screw','M4x10 Cap Screw','M4x10 Cap Screw',(#14774));
#14892=COLOUR_RGB('Black',0.12,0.14,0.17);
#14893=FILL_AREA_STYLE_COLOUR('',#14892);
#14894=FILL_AREA_STYLE('',(#14893));
#14895=SURFACE_STYLE_FILL_AREA(#14894);
#14896=SURFACE_SIDE_STYLE('',(#14895));
#14897=SURFACE_STYLE_USAGE(.BOTH.,#14896);
#14898=PRESENTATION_STYLE_ASSIGNMENT((#14897));
ENDSEC;
END-ISO-10303-21;
